ISO-10303-21;
HEADER;
/* Generated by software containing ST-Developer
 * from STEP Tools, Inc. (www.steptools.com) 
 */

FILE_DESCRIPTION(
/* description */ (''),
/* implementation_level */ '2;1');

FILE_NAME(
/* name */ 'Clamp_02.step',
/* time_stamp */ '2026-10-22T13:39:42+06:00',
/* author */ (''),
/* organization */ (''),
/* preprocessor_version */ 'ST-DEVELOPER v20.2',
/* originating_system */ 'Autodesk Translation Framework v15.15.0.0',
/* authorisation */ '');

FILE_SCHEMA (('AUTOMOTIVE_DESIGN { 1 0 10303 214 3 1 1 }'));
ENDSEC;

DATA;
#10=MECHANICAL_DESIGN_GEOMETRIC_PRESENTATION_REPRESENTATION('',(#311),#17836);
#163=SPHERICAL_SURFACE('',#10323,0.299999999999994);
#164=SPHERICAL_SURFACE('',#10334,0.3);
#165=SPHERICAL_SURFACE('',#10338,0.299999999999994);
#166=SPHERICAL_SURFACE('',#10343,0.3);
#167=SPHERICAL_SURFACE('',#10347,0.300000000000011);
#168=SPHERICAL_SURFACE('',#10351,0.300000000000003);
#169=SPHERICAL_SURFACE('',#10355,0.299999999999994);
#170=SPHERICAL_SURFACE('',#10360,0.300000000000011);
#235=TOROIDAL_SURFACE('',#10305,4.79999999999999,0.3);
#236=TOROIDAL_SURFACE('',#10311,4.79999999999998,0.3);
#237=TOROIDAL_SURFACE('',#10318,0.600000000000001,0.3);
#238=TOROIDAL_SURFACE('',#10327,0.600000000000001,0.300000000000011);
#239=TOROIDAL_SURFACE('',#10390,4.79999999999998,0.3);
#240=TOROIDAL_SURFACE('',#10395,4.79999999999999,0.3);
#271=ELLIPSE('',#10333,0.424264068711946,0.3);
#272=ELLIPSE('',#10377,0.424264068711924,0.3);
#291=SHAPE_REPRESENTATION_RELATIONSHIP('SRR','None',#17878,#301);
#301=ADVANCED_BREP_SHAPE_REPRESENTATION('',(#321),#17830);
#311=STYLED_ITEM('',(#17987),#321);
#321=MANIFOLD_SOLID_BREP('Clamp_02',#9632);
#455=CYLINDRICAL_SURFACE('',#10302,0.3);
#456=CYLINDRICAL_SURFACE('',#10309,0.3);
#457=CYLINDRICAL_SURFACE('',#10314,4.49999999999999);
#458=CYLINDRICAL_SURFACE('',#10332,0.3);
#459=CYLINDRICAL_SURFACE('',#10342,0.3);
#460=CYLINDRICAL_SURFACE('',#10359,0.3);
#461=CYLINDRICAL_SURFACE('',#10364,0.3);
#462=CYLINDRICAL_SURFACE('',#10365,0.3);
#463=CYLINDRICAL_SURFACE('',#10366,0.3);
#464=CYLINDRICAL_SURFACE('',#10367,0.3);
#465=CYLINDRICAL_SURFACE('',#10368,0.3);
#466=CYLINDRICAL_SURFACE('',#10369,0.3);
#467=CYLINDRICAL_SURFACE('',#10370,0.3);
#468=CYLINDRICAL_SURFACE('',#10371,0.3);
#469=CYLINDRICAL_SURFACE('',#10372,0.3);
#470=CYLINDRICAL_SURFACE('',#10373,0.3);
#471=CYLINDRICAL_SURFACE('',#10374,0.3);
#472=CYLINDRICAL_SURFACE('',#10375,0.3);
#473=CYLINDRICAL_SURFACE('',#10376,0.3);
#474=CYLINDRICAL_SURFACE('',#10378,0.3);
#475=CYLINDRICAL_SURFACE('',#10387,0.3);
#476=CYLINDRICAL_SURFACE('',#10393,0.3);
#477=CYLINDRICAL_SURFACE('',#10396,4.49999999999998);
#926=LINE('',#15421,#1591);
#927=LINE('',#15424,#1592);
#928=LINE('',#15435,#1593);
#929=LINE('',#15436,#1594);
#930=LINE('',#15442,#1595);
#931=LINE('',#15445,#1596);
#932=LINE('',#15448,#1597);
#933=LINE('',#15449,#1598);
#934=LINE('',#15453,#1599);
#935=LINE('',#15455,#1600);
#936=LINE('',#15457,#1601);
#937=LINE('',#15458,#1602);
#938=LINE('',#15484,#1603);
#939=LINE('',#15487,#1604);
#940=LINE('',#15502,#1605);
#941=LINE('',#15503,#1606);
#942=LINE('',#15532,#1607);
#943=LINE('',#15533,#1608);
#944=LINE('',#15542,#1609);
#945=LINE('',#15543,#1610);
#946=LINE('',#15545,#1611);
#947=LINE('',#15546,#1612);
#948=LINE('',#15548,#1613);
#949=LINE('',#15549,#1614);
#950=LINE('',#15551,#1615);
#951=LINE('',#15552,#1616);
#952=LINE('',#15554,#1617);
#953=LINE('',#15555,#1618);
#954=LINE('',#15557,#1619);
#955=LINE('',#15558,#1620);
#956=LINE('',#15560,#1621);
#957=LINE('',#15562,#1622);
#958=LINE('',#15564,#1623);
#959=LINE('',#15565,#1624);
#960=LINE('',#15567,#1625);
#961=LINE('',#15568,#1626);
#962=LINE('',#15570,#1627);
#963=LINE('',#15572,#1628);
#964=LINE('',#15575,#1629);
#965=LINE('',#15578,#1630);
#966=LINE('',#15580,#1631);
#967=LINE('',#15581,#1632);
#968=LINE('',#15583,#1633);
#969=LINE('',#15589,#1634);
#970=LINE('',#15593,#1635);
#971=LINE('',#15606,#1636);
#972=LINE('',#15609,#1637);
#1591=VECTOR('',#12428,10.);
#1592=VECTOR('',#12431,10.);
#1593=VECTOR('',#12444,10.);
#1594=VECTOR('',#12445,10.);
#1595=VECTOR('',#12454,10.);
#1596=VECTOR('',#12457,10.);
#1597=VECTOR('',#12460,10.);
#1598=VECTOR('',#12461,10.);
#1599=VECTOR('',#12464,10.);
#1600=VECTOR('',#12465,10.);
#1601=VECTOR('',#12466,10.);
#1602=VECTOR('',#12467,10.);
#1603=VECTOR('',#12498,10.);
#1604=VECTOR('',#12501,10.);
#1605=VECTOR('',#12520,10.);
#1606=VECTOR('',#12521,10.);
#1607=VECTOR('',#12556,10.);
#1608=VECTOR('',#12557,10.);
#1609=VECTOR('',#12568,10.);
#1610=VECTOR('',#12569,10.);
#1611=VECTOR('',#12572,10.);
#1612=VECTOR('',#12573,10.);
#1613=VECTOR('',#12576,10.);
#1614=VECTOR('',#12577,10.);
#1615=VECTOR('',#12580,10.);
#1616=VECTOR('',#12581,10.);
#1617=VECTOR('',#12584,10.);
#1618=VECTOR('',#12585,10.);
#1619=VECTOR('',#12588,10.);
#1620=VECTOR('',#12589,10.);
#1621=VECTOR('',#12592,10.);
#1622=VECTOR('',#12595,10.);
#1623=VECTOR('',#12598,10.);
#1624=VECTOR('',#12599,10.);
#1625=VECTOR('',#12602,10.);
#1626=VECTOR('',#12603,10.);
#1627=VECTOR('',#12606,10.);
#1628=VECTOR('',#12609,10.);
#1629=VECTOR('',#12612,10.);
#1630=VECTOR('',#12615,10.);
#1631=VECTOR('',#12618,10.);
#1632=VECTOR('',#12619,10.);
#1633=VECTOR('',#12622,10.);
#1634=VECTOR('',#12629,10.);
#1635=VECTOR('',#12632,10.);
#1636=VECTOR('',#12655,10.);
#1637=VECTOR('',#12660,10.);
#1989=FACE_BOUND('',#2932,.T.);
#1990=FACE_BOUND('',#2964,.T.);
#2296=FACE_OUTER_BOUND('',#2925,.T.);
#2297=FACE_OUTER_BOUND('',#2926,.T.);
#2298=FACE_OUTER_BOUND('',#2927,.T.);
#2299=FACE_OUTER_BOUND('',#2928,.T.);
#2300=FACE_OUTER_BOUND('',#2929,.T.);
#2301=FACE_OUTER_BOUND('',#2930,.T.);
#2302=FACE_OUTER_BOUND('',#2931,.T.);
#2303=FACE_OUTER_BOUND('',#2933,.T.);
#2304=FACE_OUTER_BOUND('',#2934,.T.);
#2305=FACE_OUTER_BOUND('',#2935,.T.);
#2306=FACE_OUTER_BOUND('',#2936,.T.);
#2307=FACE_OUTER_BOUND('',#2937,.T.);
#2308=FACE_OUTER_BOUND('',#2938,.T.);
#2309=FACE_OUTER_BOUND('',#2939,.T.);
#2310=FACE_OUTER_BOUND('',#2940,.T.);
#2311=FACE_OUTER_BOUND('',#2941,.T.);
#2312=FACE_OUTER_BOUND('',#2942,.T.);
#2313=FACE_OUTER_BOUND('',#2943,.T.);
#2314=FACE_OUTER_BOUND('',#2944,.T.);
#2315=FACE_OUTER_BOUND('',#2945,.T.);
#2316=FACE_OUTER_BOUND('',#2946,.T.);
#2317=FACE_OUTER_BOUND('',#2947,.T.);
#2318=FACE_OUTER_BOUND('',#2948,.T.);
#2319=FACE_OUTER_BOUND('',#2949,.T.);
#2320=FACE_OUTER_BOUND('',#2950,.T.);
#2321=FACE_OUTER_BOUND('',#2951,.T.);
#2322=FACE_OUTER_BOUND('',#2952,.T.);
#2323=FACE_OUTER_BOUND('',#2953,.T.);
#2324=FACE_OUTER_BOUND('',#2954,.T.);
#2325=FACE_OUTER_BOUND('',#2955,.T.);
#2326=FACE_OUTER_BOUND('',#2956,.T.);
#2327=FACE_OUTER_BOUND('',#2957,.T.);
#2328=FACE_OUTER_BOUND('',#2958,.T.);
#2329=FACE_OUTER_BOUND('',#2959,.T.);
#2330=FACE_OUTER_BOUND('',#2960,.T.);
#2331=FACE_OUTER_BOUND('',#2961,.T.);
#2332=FACE_OUTER_BOUND('',#2962,.T.);
#2333=FACE_OUTER_BOUND('',#2963,.T.);
#2334=FACE_OUTER_BOUND('',#2965,.T.);
#2335=FACE_OUTER_BOUND('',#2966,.T.);
#2336=FACE_OUTER_BOUND('',#2967,.T.);
#2337=FACE_OUTER_BOUND('',#2968,.T.);
#2338=FACE_OUTER_BOUND('',#2969,.T.);
#2339=FACE_OUTER_BOUND('',#2970,.T.);
#2340=FACE_OUTER_BOUND('',#2971,.T.);
#2341=FACE_OUTER_BOUND('',#2972,.T.);
#2342=FACE_OUTER_BOUND('',#2973,.T.);
#2925=EDGE_LOOP('',(#7231,#7232,#7233,#7234));
#2926=EDGE_LOOP('',(#7235,#7236,#7237,#7238));
#2927=EDGE_LOOP('',(#7239,#7240,#7241,#7242));
#2928=EDGE_LOOP('',(#7243,#7244,#7245,#7246));
#2929=EDGE_LOOP('',(#7247,#7248,#7249,#7250));
#2930=EDGE_LOOP('',(#7251,#7252,#7253,#7254));
#2931=EDGE_LOOP('',(#7255,#7256,#7257,#7258));
#2932=EDGE_LOOP('',(#7259,#7260,#7261,#7262));
#2933=EDGE_LOOP('',(#7263,#7264,#7265,#7266));
#2934=EDGE_LOOP('',(#7267,#7268,#7269));
#2935=EDGE_LOOP('',(#7270,#7271,#7272,#7273));
#2936=EDGE_LOOP('',(#7274,#7275,#7276,#7277));
#2937=EDGE_LOOP('',(#7278,#7279,#7280));
#2938=EDGE_LOOP('',(#7281,#7282,#7283));
#2939=EDGE_LOOP('',(#7284,#7285,#7286,#7287));
#2940=EDGE_LOOP('',(#7288,#7289,#7290));
#2941=EDGE_LOOP('',(#7291,#7292,#7293));
#2942=EDGE_LOOP('',(#7294,#7295,#7296));
#2943=EDGE_LOOP('',(#7297,#7298,#7299));
#2944=EDGE_LOOP('',(#7300,#7301,#7302,#7303));
#2945=EDGE_LOOP('',(#7304,#7305,#7306));
#2946=EDGE_LOOP('',(#7307,#7308,#7309,#7310));
#2947=EDGE_LOOP('',(#7311,#7312,#7313,#7314));
#2948=EDGE_LOOP('',(#7315,#7316,#7317,#7318));
#2949=EDGE_LOOP('',(#7319,#7320,#7321,#7322));
#2950=EDGE_LOOP('',(#7323,#7324,#7325,#7326));
#2951=EDGE_LOOP('',(#7327,#7328,#7329,#7330));
#2952=EDGE_LOOP('',(#7331,#7332,#7333,#7334));
#2953=EDGE_LOOP('',(#7335,#7336,#7337,#7338));
#2954=EDGE_LOOP('',(#7339,#7340,#7341,#7342));
#2955=EDGE_LOOP('',(#7343,#7344,#7345,#7346));
#2956=EDGE_LOOP('',(#7347,#7348,#7349,#7350));
#2957=EDGE_LOOP('',(#7351,#7352,#7353,#7354));
#2958=EDGE_LOOP('',(#7355,#7356,#7357,#7358));
#2959=EDGE_LOOP('',(#7359,#7360,#7361,#7362));
#2960=EDGE_LOOP('',(#7363,#7364,#7365,#7366));
#2961=EDGE_LOOP('',(#7367,#7368,#7369,#7370,#7371,#7372,#7373));
#2962=EDGE_LOOP('',(#7374,#7375,#7376,#7377));
#2963=EDGE_LOOP('',(#7378,#7379,#7380,#7381));
#2964=EDGE_LOOP('',(#7382,#7383,#7384,#7385));
#2965=EDGE_LOOP('',(#7386,#7387,#7388,#7389));
#2966=EDGE_LOOP('',(#7390,#7391,#7392,#7393,#7394,#7395,#7396));
#2967=EDGE_LOOP('',(#7397,#7398,#7399,#7400));
#2968=EDGE_LOOP('',(#7401,#7402,#7403,#7404));
#2969=EDGE_LOOP('',(#7405,#7406,#7407,#7408));
#2970=EDGE_LOOP('',(#7409,#7410,#7411,#7412));
#2971=EDGE_LOOP('',(#7413,#7414,#7415,#7416));
#2972=EDGE_LOOP('',(#7417,#7418,#7419,#7420));
#2973=EDGE_LOOP('',(#7421,#7422,#7423,#7424));
#3582=CIRCLE('',#10303,0.3);
#3583=CIRCLE('',#10304,0.299999999999994);
#3584=CIRCLE('',#10306,0.300000000000011);
#3585=CIRCLE('',#10307,4.49999999999999);
#3586=CIRCLE('',#10308,4.79999999999999);
#3587=CIRCLE('',#10310,0.300000000000002);
#3588=CIRCLE('',#10312,4.49999999999998);
#3589=CIRCLE('',#10313,4.79999999999998);
#3590=CIRCLE('',#10315,4.49999999999999);
#3591=CIRCLE('',#10319,0.3);
#3592=CIRCLE('',#10320,0.599999999999987);
#3593=CIRCLE('',#10321,0.300000000000011);
#3594=CIRCLE('',#10322,0.299999999999994);
#3595=CIRCLE('',#10324,0.3);
#3596=CIRCLE('',#10325,0.300000000000011);
#3597=CIRCLE('',#10326,0.299999999999994);
#3598=CIRCLE('',#10328,0.600000000000001);
#3599=CIRCLE('',#10329,0.300000000000011);
#3600=CIRCLE('',#10330,0.3);
#3601=CIRCLE('',#10331,0.299999999999976);
#3602=CIRCLE('',#10335,0.300000000000003);
#3603=CIRCLE('',#10336,0.300000000000011);
#3604=CIRCLE('',#10337,0.3);
#3605=CIRCLE('',#10339,0.3);
#3606=CIRCLE('',#10340,0.300000000000011);
#3607=CIRCLE('',#10341,0.299999999999994);
#3608=CIRCLE('',#10344,0.299999999999994);
#3609=CIRCLE('',#10345,0.300000000000011);
#3610=CIRCLE('',#10346,0.3);
#3611=CIRCLE('',#10348,0.300000000000006);
#3612=CIRCLE('',#10349,0.3);
#3613=CIRCLE('',#10350,0.300000000000011);
#3614=CIRCLE('',#10352,0.3);
#3615=CIRCLE('',#10353,0.300000000000011);
#3616=CIRCLE('',#10354,0.300000000000003);
#3617=CIRCLE('',#10356,0.300000000000011);
#3618=CIRCLE('',#10357,0.3);
#3619=CIRCLE('',#10358,0.299999999999994);
#3620=CIRCLE('',#10361,0.3);
#3621=CIRCLE('',#10362,0.300000000000001);
#3622=CIRCLE('',#10363,0.300000000000011);
#3623=CIRCLE('',#10383,4.79999999999999);
#3624=CIRCLE('',#10384,4.79999999999998);
#3625=CIRCLE('',#10388,0.3);
#3626=CIRCLE('',#10389,0.299999999999994);
#3627=CIRCLE('',#10391,0.300000000000002);
#3628=CIRCLE('',#10392,4.49999999999998);
#3629=CIRCLE('',#10394,0.300000000000002);
#4250=VERTEX_POINT('',#15417);
#4251=VERTEX_POINT('',#15418);
#4252=VERTEX_POINT('',#15420);
#4253=VERTEX_POINT('',#15422);
#4254=VERTEX_POINT('',#15426);
#4255=VERTEX_POINT('',#15427);
#4256=VERTEX_POINT('',#15432);
#4257=VERTEX_POINT('',#15433);
#4258=VERTEX_POINT('',#15441);
#4259=VERTEX_POINT('',#15443);
#4260=VERTEX_POINT('',#15447);
#4261=VERTEX_POINT('',#15451);
#4262=VERTEX_POINT('',#15452);
#4263=VERTEX_POINT('',#15454);
#4264=VERTEX_POINT('',#15456);
#4265=VERTEX_POINT('',#15460);
#4266=VERTEX_POINT('',#15462);
#4267=VERTEX_POINT('',#15464);
#4268=VERTEX_POINT('',#15468);
#4269=VERTEX_POINT('',#15469);
#4270=VERTEX_POINT('',#15471);
#4271=VERTEX_POINT('',#15475);
#4272=VERTEX_POINT('',#15476);
#4273=VERTEX_POINT('',#15479);
#4274=VERTEX_POINT('',#15483);
#4275=VERTEX_POINT('',#15485);
#4276=VERTEX_POINT('',#15489);
#4277=VERTEX_POINT('',#15490);
#4278=VERTEX_POINT('',#15495);
#4279=VERTEX_POINT('',#15496);
#4280=VERTEX_POINT('',#15498);
#4281=VERTEX_POINT('',#15505);
#4282=VERTEX_POINT('',#15506);
#4283=VERTEX_POINT('',#15508);
#4284=VERTEX_POINT('',#15512);
#4285=VERTEX_POINT('',#15514);
#4286=VERTEX_POINT('',#15518);
#4287=VERTEX_POINT('',#15519);
#4288=VERTEX_POINT('',#15521);
#4289=VERTEX_POINT('',#15525);
#4290=VERTEX_POINT('',#15526);
#4291=VERTEX_POINT('',#15528);
#4292=VERTEX_POINT('',#15535);
#4293=VERTEX_POINT('',#15536);
#4294=VERTEX_POINT('',#15538);
#4295=VERTEX_POINT('',#15574);
#4296=VERTEX_POINT('',#15576);
#4297=VERTEX_POINT('',#15587);
#4298=VERTEX_POINT('',#15588);
#4299=VERTEX_POINT('',#15590);
#4300=VERTEX_POINT('',#15592);
#4301=VERTEX_POINT('',#15601);
#5286=EDGE_CURVE('',#4250,#4251,#3582,.T.);
#5287=EDGE_CURVE('',#4252,#4250,#926,.T.);
#5288=EDGE_CURVE('',#4253,#4252,#3583,.T.);
#5289=EDGE_CURVE('',#4251,#4253,#927,.T.);
#5290=EDGE_CURVE('',#4254,#4255,#3584,.T.);
#5291=EDGE_CURVE('',#4253,#4254,#3585,.T.);
#5292=EDGE_CURVE('',#4255,#4252,#3586,.T.);
#5293=EDGE_CURVE('',#4256,#4257,#3587,.T.);
#5294=EDGE_CURVE('',#4254,#4256,#928,.T.);
#5295=EDGE_CURVE('',#4257,#4255,#929,.T.);
#5296=EDGE_CURVE('',#4256,#4251,#3588,.T.);
#5297=EDGE_CURVE('',#4250,#4257,#3589,.T.);
#5298=EDGE_CURVE('',#4258,#4254,#930,.T.);
#5299=EDGE_CURVE('',#4258,#4259,#3590,.T.);
#5300=EDGE_CURVE('',#4259,#4253,#931,.T.);
#5301=EDGE_CURVE('',#4259,#4260,#932,.T.);
#5302=EDGE_CURVE('',#4260,#4251,#933,.T.);
#5303=EDGE_CURVE('',#4261,#4262,#934,.T.);
#5304=EDGE_CURVE('',#4262,#4263,#935,.T.);
#5305=EDGE_CURVE('',#4263,#4264,#936,.T.);
#5306=EDGE_CURVE('',#4264,#4261,#937,.T.);
#5307=EDGE_CURVE('',#4264,#4265,#3591,.T.);
#5308=EDGE_CURVE('',#4266,#4265,#3592,.T.);
#5309=EDGE_CURVE('',#4266,#4267,#3593,.T.);
#5310=EDGE_CURVE('',#4267,#4264,#3594,.F.);
#5311=EDGE_CURVE('',#4268,#4269,#3595,.F.);
#5312=EDGE_CURVE('',#4269,#4270,#3596,.F.);
#5313=EDGE_CURVE('',#4270,#4268,#3597,.F.);
#5314=EDGE_CURVE('',#4271,#4272,#3598,.T.);
#5315=EDGE_CURVE('',#4271,#4261,#3599,.T.);
#5316=EDGE_CURVE('',#4261,#4273,#3600,.F.);
#5317=EDGE_CURVE('',#4273,#4272,#3601,.T.);
#5318=EDGE_CURVE('',#4274,#4273,#938,.T.);
#5319=EDGE_CURVE('',#4275,#4274,#271,.T.);
#5320=EDGE_CURVE('',#4272,#4275,#939,.T.);
#5321=EDGE_CURVE('',#4276,#4277,#3602,.F.);
#5322=EDGE_CURVE('',#4277,#4263,#3603,.F.);
#5323=EDGE_CURVE('',#4263,#4276,#3604,.F.);
#5324=EDGE_CURVE('',#4278,#4279,#3605,.F.);
#5325=EDGE_CURVE('',#4279,#4280,#3606,.F.);
#5326=EDGE_CURVE('',#4280,#4278,#3607,.F.);
#5327=EDGE_CURVE('',#4275,#4280,#940,.T.);
#5328=EDGE_CURVE('',#4278,#4274,#941,.T.);
#5329=EDGE_CURVE('',#4281,#4282,#3608,.F.);
#5330=EDGE_CURVE('',#4282,#4283,#3609,.F.);
#5331=EDGE_CURVE('',#4283,#4281,#3610,.F.);
#5332=EDGE_CURVE('',#4284,#4262,#3611,.F.);
#5333=EDGE_CURVE('',#4262,#4285,#3612,.F.);
#5334=EDGE_CURVE('',#4285,#4284,#3613,.F.);
#5335=EDGE_CURVE('',#4286,#4287,#3614,.F.);
#5336=EDGE_CURVE('',#4287,#4288,#3615,.F.);
#5337=EDGE_CURVE('',#4288,#4286,#3616,.F.);
#5338=EDGE_CURVE('',#4289,#4290,#3617,.F.);
#5339=EDGE_CURVE('',#4290,#4291,#3618,.F.);
#5340=EDGE_CURVE('',#4291,#4289,#3619,.F.);
#5341=EDGE_CURVE('',#4280,#4291,#942,.T.);
#5342=EDGE_CURVE('',#4289,#4279,#943,.T.);
#5343=EDGE_CURVE('',#4292,#4293,#3620,.F.);
#5344=EDGE_CURVE('',#4293,#4294,#3621,.F.);
#5345=EDGE_CURVE('',#4294,#4292,#3622,.F.);
#5346=EDGE_CURVE('',#4292,#4290,#944,.T.);
#5347=EDGE_CURVE('',#4291,#4294,#945,.T.);
#5348=EDGE_CURVE('',#4284,#4293,#946,.T.);
#5349=EDGE_CURVE('',#4294,#4285,#947,.T.);
#5350=EDGE_CURVE('',#4293,#4288,#948,.T.);
#5351=EDGE_CURVE('',#4286,#4292,#949,.T.);
#5352=EDGE_CURVE('',#4290,#4283,#950,.T.);
#5353=EDGE_CURVE('',#4281,#4289,#951,.T.);
#5354=EDGE_CURVE('',#4288,#4276,#952,.T.);
#5355=EDGE_CURVE('',#4277,#4287,#953,.T.);
#5356=EDGE_CURVE('',#4283,#4286,#954,.T.);
#5357=EDGE_CURVE('',#4287,#4282,#955,.T.);
#5358=EDGE_CURVE('',#4285,#4271,#956,.T.);
#5359=EDGE_CURVE('',#4276,#4284,#957,.T.);
#5360=EDGE_CURVE('',#4270,#4281,#958,.T.);
#5361=EDGE_CURVE('',#4282,#4269,#959,.T.);
#5362=EDGE_CURVE('',#4279,#4270,#960,.T.);
#5363=EDGE_CURVE('',#4268,#4278,#961,.T.);
#5364=EDGE_CURVE('',#4265,#4277,#962,.T.);
#5365=EDGE_CURVE('',#4273,#4267,#963,.T.);
#5366=EDGE_CURVE('',#4295,#4268,#964,.T.);
#5367=EDGE_CURVE('',#4296,#4295,#272,.T.);
#5368=EDGE_CURVE('',#4269,#4296,#965,.T.);
#5369=EDGE_CURVE('',#4296,#4266,#966,.T.);
#5370=EDGE_CURVE('',#4267,#4295,#967,.T.);
#5371=EDGE_CURVE('',#4274,#4295,#968,.T.);
#5372=EDGE_CURVE('',#4297,#4298,#969,.T.);
#5373=EDGE_CURVE('',#4298,#4299,#3623,.T.);
#5374=EDGE_CURVE('',#4299,#4300,#970,.T.);
#5375=EDGE_CURVE('',#4300,#4297,#3624,.T.);
#5376=EDGE_CURVE('',#4298,#4259,#3625,.T.);
#5377=EDGE_CURVE('',#4260,#4297,#3626,.T.);
#5378=EDGE_CURVE('',#4301,#4300,#3627,.T.);
#5379=EDGE_CURVE('',#4260,#4301,#3628,.T.);
#5380=EDGE_CURVE('',#4258,#4299,#3629,.T.);
#5381=EDGE_CURVE('',#4301,#4258,#971,.T.);
#5382=EDGE_CURVE('',#4301,#4256,#972,.T.);
#7231=ORIENTED_EDGE('',*,*,#5286,.F.);
#7232=ORIENTED_EDGE('',*,*,#5287,.F.);
#7233=ORIENTED_EDGE('',*,*,#5288,.F.);
#7234=ORIENTED_EDGE('',*,*,#5289,.F.);
#7235=ORIENTED_EDGE('',*,*,#5290,.F.);
#7236=ORIENTED_EDGE('',*,*,#5291,.F.);
#7237=ORIENTED_EDGE('',*,*,#5288,.T.);
#7238=ORIENTED_EDGE('',*,*,#5292,.F.);
#7239=ORIENTED_EDGE('',*,*,#5293,.F.);
#7240=ORIENTED_EDGE('',*,*,#5294,.F.);
#7241=ORIENTED_EDGE('',*,*,#5290,.T.);
#7242=ORIENTED_EDGE('',*,*,#5295,.F.);
#7243=ORIENTED_EDGE('',*,*,#5286,.T.);
#7244=ORIENTED_EDGE('',*,*,#5296,.F.);
#7245=ORIENTED_EDGE('',*,*,#5293,.T.);
#7246=ORIENTED_EDGE('',*,*,#5297,.F.);
#7247=ORIENTED_EDGE('',*,*,#5291,.T.);
#7248=ORIENTED_EDGE('',*,*,#5298,.F.);
#7249=ORIENTED_EDGE('',*,*,#5299,.T.);
#7250=ORIENTED_EDGE('',*,*,#5300,.T.);
#7251=ORIENTED_EDGE('',*,*,#5289,.T.);
#7252=ORIENTED_EDGE('',*,*,#5300,.F.);
#7253=ORIENTED_EDGE('',*,*,#5301,.T.);
#7254=ORIENTED_EDGE('',*,*,#5302,.T.);
#7255=ORIENTED_EDGE('',*,*,#5303,.T.);
#7256=ORIENTED_EDGE('',*,*,#5304,.T.);
#7257=ORIENTED_EDGE('',*,*,#5305,.T.);
#7258=ORIENTED_EDGE('',*,*,#5306,.T.);
#7259=ORIENTED_EDGE('',*,*,#5287,.T.);
#7260=ORIENTED_EDGE('',*,*,#5297,.T.);
#7261=ORIENTED_EDGE('',*,*,#5295,.T.);
#7262=ORIENTED_EDGE('',*,*,#5292,.T.);
#7263=ORIENTED_EDGE('',*,*,#5307,.T.);
#7264=ORIENTED_EDGE('',*,*,#5308,.F.);
#7265=ORIENTED_EDGE('',*,*,#5309,.T.);
#7266=ORIENTED_EDGE('',*,*,#5310,.T.);
#7267=ORIENTED_EDGE('',*,*,#5311,.T.);
#7268=ORIENTED_EDGE('',*,*,#5312,.T.);
#7269=ORIENTED_EDGE('',*,*,#5313,.T.);
#7270=ORIENTED_EDGE('',*,*,#5314,.F.);
#7271=ORIENTED_EDGE('',*,*,#5315,.T.);
#7272=ORIENTED_EDGE('',*,*,#5316,.T.);
#7273=ORIENTED_EDGE('',*,*,#5317,.T.);
#7274=ORIENTED_EDGE('',*,*,#5318,.F.);
#7275=ORIENTED_EDGE('',*,*,#5319,.F.);
#7276=ORIENTED_EDGE('',*,*,#5320,.F.);
#7277=ORIENTED_EDGE('',*,*,#5317,.F.);
#7278=ORIENTED_EDGE('',*,*,#5321,.T.);
#7279=ORIENTED_EDGE('',*,*,#5322,.T.);
#7280=ORIENTED_EDGE('',*,*,#5323,.T.);
#7281=ORIENTED_EDGE('',*,*,#5324,.T.);
#7282=ORIENTED_EDGE('',*,*,#5325,.T.);
#7283=ORIENTED_EDGE('',*,*,#5326,.T.);
#7284=ORIENTED_EDGE('',*,*,#5327,.F.);
#7285=ORIENTED_EDGE('',*,*,#5319,.T.);
#7286=ORIENTED_EDGE('',*,*,#5328,.F.);
#7287=ORIENTED_EDGE('',*,*,#5326,.F.);
#7288=ORIENTED_EDGE('',*,*,#5329,.T.);
#7289=ORIENTED_EDGE('',*,*,#5330,.T.);
#7290=ORIENTED_EDGE('',*,*,#5331,.T.);
#7291=ORIENTED_EDGE('',*,*,#5332,.T.);
#7292=ORIENTED_EDGE('',*,*,#5333,.T.);
#7293=ORIENTED_EDGE('',*,*,#5334,.T.);
#7294=ORIENTED_EDGE('',*,*,#5335,.T.);
#7295=ORIENTED_EDGE('',*,*,#5336,.T.);
#7296=ORIENTED_EDGE('',*,*,#5337,.T.);
#7297=ORIENTED_EDGE('',*,*,#5338,.T.);
#7298=ORIENTED_EDGE('',*,*,#5339,.T.);
#7299=ORIENTED_EDGE('',*,*,#5340,.T.);
#7300=ORIENTED_EDGE('',*,*,#5340,.F.);
#7301=ORIENTED_EDGE('',*,*,#5341,.F.);
#7302=ORIENTED_EDGE('',*,*,#5325,.F.);
#7303=ORIENTED_EDGE('',*,*,#5342,.F.);
#7304=ORIENTED_EDGE('',*,*,#5343,.T.);
#7305=ORIENTED_EDGE('',*,*,#5344,.T.);
#7306=ORIENTED_EDGE('',*,*,#5345,.T.);
#7307=ORIENTED_EDGE('',*,*,#5339,.F.);
#7308=ORIENTED_EDGE('',*,*,#5346,.F.);
#7309=ORIENTED_EDGE('',*,*,#5345,.F.);
#7310=ORIENTED_EDGE('',*,*,#5347,.F.);
#7311=ORIENTED_EDGE('',*,*,#5344,.F.);
#7312=ORIENTED_EDGE('',*,*,#5348,.F.);
#7313=ORIENTED_EDGE('',*,*,#5334,.F.);
#7314=ORIENTED_EDGE('',*,*,#5349,.F.);
#7315=ORIENTED_EDGE('',*,*,#5337,.F.);
#7316=ORIENTED_EDGE('',*,*,#5350,.F.);
#7317=ORIENTED_EDGE('',*,*,#5343,.F.);
#7318=ORIENTED_EDGE('',*,*,#5351,.F.);
#7319=ORIENTED_EDGE('',*,*,#5331,.F.);
#7320=ORIENTED_EDGE('',*,*,#5352,.F.);
#7321=ORIENTED_EDGE('',*,*,#5338,.F.);
#7322=ORIENTED_EDGE('',*,*,#5353,.F.);
#7323=ORIENTED_EDGE('',*,*,#5321,.F.);
#7324=ORIENTED_EDGE('',*,*,#5354,.F.);
#7325=ORIENTED_EDGE('',*,*,#5336,.F.);
#7326=ORIENTED_EDGE('',*,*,#5355,.F.);
#7327=ORIENTED_EDGE('',*,*,#5335,.F.);
#7328=ORIENTED_EDGE('',*,*,#5356,.F.);
#7329=ORIENTED_EDGE('',*,*,#5330,.F.);
#7330=ORIENTED_EDGE('',*,*,#5357,.F.);
#7331=ORIENTED_EDGE('',*,*,#5333,.F.);
#7332=ORIENTED_EDGE('',*,*,#5303,.F.);
#7333=ORIENTED_EDGE('',*,*,#5315,.F.);
#7334=ORIENTED_EDGE('',*,*,#5358,.F.);
#7335=ORIENTED_EDGE('',*,*,#5323,.F.);
#7336=ORIENTED_EDGE('',*,*,#5304,.F.);
#7337=ORIENTED_EDGE('',*,*,#5332,.F.);
#7338=ORIENTED_EDGE('',*,*,#5359,.F.);
#7339=ORIENTED_EDGE('',*,*,#5329,.F.);
#7340=ORIENTED_EDGE('',*,*,#5360,.F.);
#7341=ORIENTED_EDGE('',*,*,#5312,.F.);
#7342=ORIENTED_EDGE('',*,*,#5361,.F.);
#7343=ORIENTED_EDGE('',*,*,#5313,.F.);
#7344=ORIENTED_EDGE('',*,*,#5362,.F.);
#7345=ORIENTED_EDGE('',*,*,#5324,.F.);
#7346=ORIENTED_EDGE('',*,*,#5363,.F.);
#7347=ORIENTED_EDGE('',*,*,#5307,.F.);
#7348=ORIENTED_EDGE('',*,*,#5305,.F.);
#7349=ORIENTED_EDGE('',*,*,#5322,.F.);
#7350=ORIENTED_EDGE('',*,*,#5364,.F.);
#7351=ORIENTED_EDGE('',*,*,#5310,.F.);
#7352=ORIENTED_EDGE('',*,*,#5365,.F.);
#7353=ORIENTED_EDGE('',*,*,#5316,.F.);
#7354=ORIENTED_EDGE('',*,*,#5306,.F.);
#7355=ORIENTED_EDGE('',*,*,#5366,.F.);
#7356=ORIENTED_EDGE('',*,*,#5367,.F.);
#7357=ORIENTED_EDGE('',*,*,#5368,.F.);
#7358=ORIENTED_EDGE('',*,*,#5311,.F.);
#7359=ORIENTED_EDGE('',*,*,#5369,.F.);
#7360=ORIENTED_EDGE('',*,*,#5367,.T.);
#7361=ORIENTED_EDGE('',*,*,#5370,.F.);
#7362=ORIENTED_EDGE('',*,*,#5309,.F.);
#7363=ORIENTED_EDGE('',*,*,#5370,.T.);
#7364=ORIENTED_EDGE('',*,*,#5371,.F.);
#7365=ORIENTED_EDGE('',*,*,#5318,.T.);
#7366=ORIENTED_EDGE('',*,*,#5365,.T.);
#7367=ORIENTED_EDGE('',*,*,#5314,.T.);
#7368=ORIENTED_EDGE('',*,*,#5320,.T.);
#7369=ORIENTED_EDGE('',*,*,#5327,.T.);
#7370=ORIENTED_EDGE('',*,*,#5341,.T.);
#7371=ORIENTED_EDGE('',*,*,#5347,.T.);
#7372=ORIENTED_EDGE('',*,*,#5349,.T.);
#7373=ORIENTED_EDGE('',*,*,#5358,.T.);
#7374=ORIENTED_EDGE('',*,*,#5342,.T.);
#7375=ORIENTED_EDGE('',*,*,#5362,.T.);
#7376=ORIENTED_EDGE('',*,*,#5360,.T.);
#7377=ORIENTED_EDGE('',*,*,#5353,.T.);
#7378=ORIENTED_EDGE('',*,*,#5346,.T.);
#7379=ORIENTED_EDGE('',*,*,#5352,.T.);
#7380=ORIENTED_EDGE('',*,*,#5356,.T.);
#7381=ORIENTED_EDGE('',*,*,#5351,.T.);
#7382=ORIENTED_EDGE('',*,*,#5372,.T.);
#7383=ORIENTED_EDGE('',*,*,#5373,.T.);
#7384=ORIENTED_EDGE('',*,*,#5374,.T.);
#7385=ORIENTED_EDGE('',*,*,#5375,.T.);
#7386=ORIENTED_EDGE('',*,*,#5348,.T.);
#7387=ORIENTED_EDGE('',*,*,#5350,.T.);
#7388=ORIENTED_EDGE('',*,*,#5354,.T.);
#7389=ORIENTED_EDGE('',*,*,#5359,.T.);
#7390=ORIENTED_EDGE('',*,*,#5355,.T.);
#7391=ORIENTED_EDGE('',*,*,#5357,.T.);
#7392=ORIENTED_EDGE('',*,*,#5361,.T.);
#7393=ORIENTED_EDGE('',*,*,#5368,.T.);
#7394=ORIENTED_EDGE('',*,*,#5369,.T.);
#7395=ORIENTED_EDGE('',*,*,#5308,.T.);
#7396=ORIENTED_EDGE('',*,*,#5364,.T.);
#7397=ORIENTED_EDGE('',*,*,#5376,.F.);
#7398=ORIENTED_EDGE('',*,*,#5372,.F.);
#7399=ORIENTED_EDGE('',*,*,#5377,.F.);
#7400=ORIENTED_EDGE('',*,*,#5301,.F.);
#7401=ORIENTED_EDGE('',*,*,#5378,.F.);
#7402=ORIENTED_EDGE('',*,*,#5379,.F.);
#7403=ORIENTED_EDGE('',*,*,#5377,.T.);
#7404=ORIENTED_EDGE('',*,*,#5375,.F.);
#7405=ORIENTED_EDGE('',*,*,#5380,.F.);
#7406=ORIENTED_EDGE('',*,*,#5381,.F.);
#7407=ORIENTED_EDGE('',*,*,#5378,.T.);
#7408=ORIENTED_EDGE('',*,*,#5374,.F.);
#7409=ORIENTED_EDGE('',*,*,#5376,.T.);
#7410=ORIENTED_EDGE('',*,*,#5299,.F.);
#7411=ORIENTED_EDGE('',*,*,#5380,.T.);
#7412=ORIENTED_EDGE('',*,*,#5373,.F.);
#7413=ORIENTED_EDGE('',*,*,#5296,.T.);
#7414=ORIENTED_EDGE('',*,*,#5302,.F.);
#7415=ORIENTED_EDGE('',*,*,#5379,.T.);
#7416=ORIENTED_EDGE('',*,*,#5382,.T.);
#7417=ORIENTED_EDGE('',*,*,#5294,.T.);
#7418=ORIENTED_EDGE('',*,*,#5382,.F.);
#7419=ORIENTED_EDGE('',*,*,#5381,.T.);
#7420=ORIENTED_EDGE('',*,*,#5298,.T.);
#7421=ORIENTED_EDGE('',*,*,#5366,.T.);
#7422=ORIENTED_EDGE('',*,*,#5363,.T.);
#7423=ORIENTED_EDGE('',*,*,#5328,.T.);
#7424=ORIENTED_EDGE('',*,*,#5371,.T.);
#8936=PLANE('',#10316);
#8937=PLANE('',#10317);
#8938=PLANE('',#10379);
#8939=PLANE('',#10380);
#8940=PLANE('',#10381);
#8941=PLANE('',#10382);
#8942=PLANE('',#10385);
#8943=PLANE('',#10386);
#8944=PLANE('',#10397);
#8945=PLANE('',#10398);
#9283=ADVANCED_FACE('',(#2296),#455,.T.);
#9284=ADVANCED_FACE('',(#2297),#235,.T.);
#9285=ADVANCED_FACE('',(#2298),#456,.T.);
#9286=ADVANCED_FACE('',(#2299),#236,.T.);
#9287=ADVANCED_FACE('',(#2300),#457,.F.);
#9288=ADVANCED_FACE('',(#2301),#8936,.T.);
#9289=ADVANCED_FACE('',(#2302,#1989),#8937,.F.);
#9290=ADVANCED_FACE('',(#2303),#237,.T.);
#9291=ADVANCED_FACE('',(#2304),#163,.T.);
#9292=ADVANCED_FACE('',(#2305),#238,.T.);
#9293=ADVANCED_FACE('',(#2306),#458,.T.);
#9294=ADVANCED_FACE('',(#2307),#164,.T.);
#9295=ADVANCED_FACE('',(#2308),#165,.T.);
#9296=ADVANCED_FACE('',(#2309),#459,.T.);
#9297=ADVANCED_FACE('',(#2310),#166,.T.);
#9298=ADVANCED_FACE('',(#2311),#167,.T.);
#9299=ADVANCED_FACE('',(#2312),#168,.T.);
#9300=ADVANCED_FACE('',(#2313),#169,.T.);
#9301=ADVANCED_FACE('',(#2314),#460,.T.);
#9302=ADVANCED_FACE('',(#2315),#170,.T.);
#9303=ADVANCED_FACE('',(#2316),#461,.T.);
#9304=ADVANCED_FACE('',(#2317),#462,.T.);
#9305=ADVANCED_FACE('',(#2318),#463,.T.);
#9306=ADVANCED_FACE('',(#2319),#464,.T.);
#9307=ADVANCED_FACE('',(#2320),#465,.T.);
#9308=ADVANCED_FACE('',(#2321),#466,.T.);
#9309=ADVANCED_FACE('',(#2322),#467,.T.);
#9310=ADVANCED_FACE('',(#2323),#468,.T.);
#9311=ADVANCED_FACE('',(#2324),#469,.T.);
#9312=ADVANCED_FACE('',(#2325),#470,.T.);
#9313=ADVANCED_FACE('',(#2326),#471,.T.);
#9314=ADVANCED_FACE('',(#2327),#472,.F.);
#9315=ADVANCED_FACE('',(#2328),#473,.T.);
#9316=ADVANCED_FACE('',(#2329),#474,.T.);
#9317=ADVANCED_FACE('',(#2330),#8938,.F.);
#9318=ADVANCED_FACE('',(#2331),#8939,.T.);
#9319=ADVANCED_FACE('',(#2332),#8940,.F.);
#9320=ADVANCED_FACE('',(#2333,#1990),#8941,.F.);
#9321=ADVANCED_FACE('',(#2334),#8942,.F.);
#9322=ADVANCED_FACE('',(#2335),#8943,.F.);
#9323=ADVANCED_FACE('',(#2336),#475,.T.);
#9324=ADVANCED_FACE('',(#2337),#239,.T.);
#9325=ADVANCED_FACE('',(#2338),#476,.T.);
#9326=ADVANCED_FACE('',(#2339),#240,.T.);
#9327=ADVANCED_FACE('',(#2340),#477,.F.);
#9328=ADVANCED_FACE('',(#2341),#8944,.T.);
#9329=ADVANCED_FACE('',(#2342),#8945,.F.);
#9632=CLOSED_SHELL('',(#9283,#9284,#9285,#9286,#9287,#9288,#9289,#9290,
#9291,#9292,#9293,#9294,#9295,#9296,#9297,#9298,#9299,#9300,#9301,#9302,
#9303,#9304,#9305,#9306,#9307,#9308,#9309,#9310,#9311,#9312,#9313,#9314,
#9315,#9316,#9317,#9318,#9319,#9320,#9321,#9322,#9323,#9324,#9325,#9326,
#9327,#9328,#9329));
#10301=AXIS2_PLACEMENT_3D('',#15415,#12422,#12423);
#10302=AXIS2_PLACEMENT_3D('',#15416,#12424,#12425);
#10303=AXIS2_PLACEMENT_3D('',#15419,#12426,#12427);
#10304=AXIS2_PLACEMENT_3D('',#15423,#12429,#12430);
#10305=AXIS2_PLACEMENT_3D('',#15425,#12432,#12433);
#10306=AXIS2_PLACEMENT_3D('',#15428,#12434,#12435);
#10307=AXIS2_PLACEMENT_3D('',#15429,#12436,#12437);
#10308=AXIS2_PLACEMENT_3D('',#15430,#12438,#12439);
#10309=AXIS2_PLACEMENT_3D('',#15431,#12440,#12441);
#10310=AXIS2_PLACEMENT_3D('',#15434,#12442,#12443);
#10311=AXIS2_PLACEMENT_3D('',#15437,#12446,#12447);
#10312=AXIS2_PLACEMENT_3D('',#15438,#12448,#12449);
#10313=AXIS2_PLACEMENT_3D('',#15439,#12450,#12451);
#10314=AXIS2_PLACEMENT_3D('',#15440,#12452,#12453);
#10315=AXIS2_PLACEMENT_3D('',#15444,#12455,#12456);
#10316=AXIS2_PLACEMENT_3D('',#15446,#12458,#12459);
#10317=AXIS2_PLACEMENT_3D('',#15450,#12462,#12463);
#10318=AXIS2_PLACEMENT_3D('',#15459,#12468,#12469);
#10319=AXIS2_PLACEMENT_3D('',#15461,#12470,#12471);
#10320=AXIS2_PLACEMENT_3D('',#15463,#12472,#12473);
#10321=AXIS2_PLACEMENT_3D('',#15465,#12474,#12475);
#10322=AXIS2_PLACEMENT_3D('',#15466,#12476,#12477);
#10323=AXIS2_PLACEMENT_3D('',#15467,#12478,#12479);
#10324=AXIS2_PLACEMENT_3D('',#15470,#12480,#12481);
#10325=AXIS2_PLACEMENT_3D('',#15472,#12482,#12483);
#10326=AXIS2_PLACEMENT_3D('',#15473,#12484,#12485);
#10327=AXIS2_PLACEMENT_3D('',#15474,#12486,#12487);
#10328=AXIS2_PLACEMENT_3D('',#15477,#12488,#12489);
#10329=AXIS2_PLACEMENT_3D('',#15478,#12490,#12491);
#10330=AXIS2_PLACEMENT_3D('',#15480,#12492,#12493);
#10331=AXIS2_PLACEMENT_3D('',#15481,#12494,#12495);
#10332=AXIS2_PLACEMENT_3D('',#15482,#12496,#12497);
#10333=AXIS2_PLACEMENT_3D('',#15486,#12499,#12500);
#10334=AXIS2_PLACEMENT_3D('',#15488,#12502,#12503);
#10335=AXIS2_PLACEMENT_3D('',#15491,#12504,#12505);
#10336=AXIS2_PLACEMENT_3D('',#15492,#12506,#12507);
#10337=AXIS2_PLACEMENT_3D('',#15493,#12508,#12509);
#10338=AXIS2_PLACEMENT_3D('',#15494,#12510,#12511);
#10339=AXIS2_PLACEMENT_3D('',#15497,#12512,#12513);
#10340=AXIS2_PLACEMENT_3D('',#15499,#12514,#12515);
#10341=AXIS2_PLACEMENT_3D('',#15500,#12516,#12517);
#10342=AXIS2_PLACEMENT_3D('',#15501,#12518,#12519);
#10343=AXIS2_PLACEMENT_3D('',#15504,#12522,#12523);
#10344=AXIS2_PLACEMENT_3D('',#15507,#12524,#12525);
#10345=AXIS2_PLACEMENT_3D('',#15509,#12526,#12527);
#10346=AXIS2_PLACEMENT_3D('',#15510,#12528,#12529);
#10347=AXIS2_PLACEMENT_3D('',#15511,#12530,#12531);
#10348=AXIS2_PLACEMENT_3D('',#15513,#12532,#12533);
#10349=AXIS2_PLACEMENT_3D('',#15515,#12534,#12535);
#10350=AXIS2_PLACEMENT_3D('',#15516,#12536,#12537);
#10351=AXIS2_PLACEMENT_3D('',#15517,#12538,#12539);
#10352=AXIS2_PLACEMENT_3D('',#15520,#12540,#12541);
#10353=AXIS2_PLACEMENT_3D('',#15522,#12542,#12543);
#10354=AXIS2_PLACEMENT_3D('',#15523,#12544,#12545);
#10355=AXIS2_PLACEMENT_3D('',#15524,#12546,#12547);
#10356=AXIS2_PLACEMENT_3D('',#15527,#12548,#12549);
#10357=AXIS2_PLACEMENT_3D('',#15529,#12550,#12551);
#10358=AXIS2_PLACEMENT_3D('',#15530,#12552,#12553);
#10359=AXIS2_PLACEMENT_3D('',#15531,#12554,#12555);
#10360=AXIS2_PLACEMENT_3D('',#15534,#12558,#12559);
#10361=AXIS2_PLACEMENT_3D('',#15537,#12560,#12561);
#10362=AXIS2_PLACEMENT_3D('',#15539,#12562,#12563);
#10363=AXIS2_PLACEMENT_3D('',#15540,#12564,#12565);
#10364=AXIS2_PLACEMENT_3D('',#15541,#12566,#12567);
#10365=AXIS2_PLACEMENT_3D('',#15544,#12570,#12571);
#10366=AXIS2_PLACEMENT_3D('',#15547,#12574,#12575);
#10367=AXIS2_PLACEMENT_3D('',#15550,#12578,#12579);
#10368=AXIS2_PLACEMENT_3D('',#15553,#12582,#12583);
#10369=AXIS2_PLACEMENT_3D('',#15556,#12586,#12587);
#10370=AXIS2_PLACEMENT_3D('',#15559,#12590,#12591);
#10371=AXIS2_PLACEMENT_3D('',#15561,#12593,#12594);
#10372=AXIS2_PLACEMENT_3D('',#15563,#12596,#12597);
#10373=AXIS2_PLACEMENT_3D('',#15566,#12600,#12601);
#10374=AXIS2_PLACEMENT_3D('',#15569,#12604,#12605);
#10375=AXIS2_PLACEMENT_3D('',#15571,#12607,#12608);
#10376=AXIS2_PLACEMENT_3D('',#15573,#12610,#12611);
#10377=AXIS2_PLACEMENT_3D('',#15577,#12613,#12614);
#10378=AXIS2_PLACEMENT_3D('',#15579,#12616,#12617);
#10379=AXIS2_PLACEMENT_3D('',#15582,#12620,#12621);
#10380=AXIS2_PLACEMENT_3D('',#15584,#12623,#12624);
#10381=AXIS2_PLACEMENT_3D('',#15585,#12625,#12626);
#10382=AXIS2_PLACEMENT_3D('',#15586,#12627,#12628);
#10383=AXIS2_PLACEMENT_3D('',#15591,#12630,#12631);
#10384=AXIS2_PLACEMENT_3D('',#15594,#12633,#12634);
#10385=AXIS2_PLACEMENT_3D('',#15595,#12635,#12636);
#10386=AXIS2_PLACEMENT_3D('',#15596,#12637,#12638);
#10387=AXIS2_PLACEMENT_3D('',#15597,#12639,#12640);
#10388=AXIS2_PLACEMENT_3D('',#15598,#12641,#12642);
#10389=AXIS2_PLACEMENT_3D('',#15599,#12643,#12644);
#10390=AXIS2_PLACEMENT_3D('',#15600,#12645,#12646);
#10391=AXIS2_PLACEMENT_3D('',#15602,#12647,#12648);
#10392=AXIS2_PLACEMENT_3D('',#15603,#12649,#12650);
#10393=AXIS2_PLACEMENT_3D('',#15604,#12651,#12652);
#10394=AXIS2_PLACEMENT_3D('',#15605,#12653,#12654);
#10395=AXIS2_PLACEMENT_3D('',#15607,#12656,#12657);
#10396=AXIS2_PLACEMENT_3D('',#15608,#12658,#12659);
#10397=AXIS2_PLACEMENT_3D('',#15610,#12661,#12662);
#10398=AXIS2_PLACEMENT_3D('',#15611,#12663,#12664);
#12422=DIRECTION('axis',(0.,0.,1.));
#12423=DIRECTION('refdir',(1.,0.,0.));
#12424=DIRECTION('center_axis',(-1.,0.,0.));
#12425=DIRECTION('ref_axis',(0.,-0.707106781186519,-0.707106781186576));
#12426=DIRECTION('center_axis',(-1.,0.,0.));
#12427=DIRECTION('ref_axis',(0.,0.,-1.));
#12428=DIRECTION('',(-1.,0.,0.));
#12429=DIRECTION('center_axis',(1.,0.,0.));
#12430=DIRECTION('ref_axis',(0.,-1.,0.));
#12431=DIRECTION('',(1.,0.,0.));
#12432=DIRECTION('center_axis',(0.,0.,1.));
#12433=DIRECTION('ref_axis',(1.,0.,0.));
#12434=DIRECTION('center_axis',(-1.,0.,0.));
#12435=DIRECTION('ref_axis',(0.,1.,0.));
#12436=DIRECTION('center_axis',(0.,0.,-1.));
#12437=DIRECTION('ref_axis',(1.,0.,0.));
#12438=DIRECTION('center_axis',(0.,0.,1.));
#12439=DIRECTION('ref_axis',(1.,0.,0.));
#12440=DIRECTION('center_axis',(1.,0.,0.));
#12441=DIRECTION('ref_axis',(0.,0.707106781186561,-0.707106781186534));
#12442=DIRECTION('center_axis',(-1.,0.,0.));
#12443=DIRECTION('ref_axis',(0.,1.,0.));
#12444=DIRECTION('',(-1.,0.,0.));
#12445=DIRECTION('',(1.,0.,0.));
#12446=DIRECTION('center_axis',(0.,0.,1.));
#12447=DIRECTION('ref_axis',(-1.,0.,0.));
#12448=DIRECTION('center_axis',(0.,0.,-1.));
#12449=DIRECTION('ref_axis',(-1.,0.,0.));
#12450=DIRECTION('center_axis',(0.,0.,1.));
#12451=DIRECTION('ref_axis',(-1.,0.,0.));
#12452=DIRECTION('center_axis',(0.,0.,1.));
#12453=DIRECTION('ref_axis',(0.,1.,0.));
#12454=DIRECTION('',(0.,0.,-1.));
#12455=DIRECTION('center_axis',(0.,0.,1.));
#12456=DIRECTION('ref_axis',(1.,0.,0.));
#12457=DIRECTION('',(0.,0.,-1.));
#12458=DIRECTION('center_axis',(0.,-1.,0.));
#12459=DIRECTION('ref_axis',(-1.,0.,0.));
#12460=DIRECTION('',(-1.,0.,0.));
#12461=DIRECTION('',(0.,0.,-1.));
#12462=DIRECTION('center_axis',(0.,0.,1.));
#12463=DIRECTION('ref_axis',(-1.,0.,0.));
#12464=DIRECTION('',(1.,0.,0.));
#12465=DIRECTION('',(0.,-1.,0.));
#12466=DIRECTION('',(-1.,0.,0.));
#12467=DIRECTION('',(0.,1.,0.));
#12468=DIRECTION('center_axis',(0.,1.,0.));
#12469=DIRECTION('ref_axis',(0.,0.,-1.));
#12470=DIRECTION('center_axis',(-1.,0.,0.));
#12471=DIRECTION('ref_axis',(0.,0.,-1.));
#12472=DIRECTION('center_axis',(0.,1.,0.));
#12473=DIRECTION('ref_axis',(-0.70710678118654,0.,0.707106781186555));
#12474=DIRECTION('center_axis',(0.,0.,1.));
#12475=DIRECTION('ref_axis',(0.,-1.,0.));
#12476=DIRECTION('center_axis',(0.,-1.,0.));
#12477=DIRECTION('ref_axis',(-1.,0.,0.));
#12478=DIRECTION('center_axis',(-0.816496580927734,0.408248290463867,0.408248290463843));
#12479=DIRECTION('ref_axis',(-0.577350269189598,-0.577350269189645,-0.577350269189634));
#12480=DIRECTION('center_axis',(1.,0.,0.));
#12481=DIRECTION('ref_axis',(0.,0.,-1.));
#12482=DIRECTION('center_axis',(9.25185853854317E-16,0.,1.));
#12483=DIRECTION('ref_axis',(0.,-1.,0.));
#12484=DIRECTION('center_axis',(0.,1.,0.));
#12485=DIRECTION('ref_axis',(-1.,0.,0.));
#12486=DIRECTION('center_axis',(0.,1.,0.));
#12487=DIRECTION('ref_axis',(0.,0.,-1.));
#12488=DIRECTION('center_axis',(0.,-1.,0.));
#12489=DIRECTION('ref_axis',(-0.70710678118654,0.,0.707106781186555));
#12490=DIRECTION('center_axis',(-1.,0.,0.));
#12491=DIRECTION('ref_axis',(0.,1.,0.));
#12492=DIRECTION('center_axis',(5.92118946466763E-14,1.,0.));
#12493=DIRECTION('ref_axis',(0.,0.,1.));
#12494=DIRECTION('center_axis',(0.,0.,1.));
#12495=DIRECTION('ref_axis',(1.,0.,0.));
#12496=DIRECTION('center_axis',(0.,0.,1.));
#12497=DIRECTION('ref_axis',(0.707106781186547,0.707106781186547,0.));
#12498=DIRECTION('',(0.,0.,1.));
#12499=DIRECTION('center_axis',(-0.707106781186576,0.,-0.707106781186519));
#12500=DIRECTION('ref_axis',(-0.707106781186519,0.,0.707106781186576));
#12501=DIRECTION('',(0.,0.,-1.));
#12502=DIRECTION('center_axis',(-0.827465426020362,-0.538877990790925,-0.157833709270471));
#12503=DIRECTION('ref_axis',(0.561516668266355,-0.794104487760816,-0.232587819494453));
#12504=DIRECTION('center_axis',(-0.707106781186544,-3.663549070262E-14,
0.707106781186551));
#12505=DIRECTION('ref_axis',(0.707106781186551,0.,0.707106781186544));
#12506=DIRECTION('center_axis',(-1.,0.,2.96059473233375E-14));
#12507=DIRECTION('ref_axis',(0.,-1.,0.));
#12508=DIRECTION('center_axis',(0.,1.,0.));
#12509=DIRECTION('ref_axis',(0.,0.,-1.));
#12510=DIRECTION('center_axis',(0.408248290463871,-0.408248290463824,-0.816496580927742));
#12511=DIRECTION('ref_axis',(-0.577350269189681,0.577350269189586,-0.57735026918961));
#12512=DIRECTION('center_axis',(0.,-1.,0.));
#12513=DIRECTION('ref_axis',(0.,0.,-1.));
#12514=DIRECTION('center_axis',(0.,-9.25185853854317E-16,1.));
#12515=DIRECTION('ref_axis',(-1.,0.,0.));
#12516=DIRECTION('center_axis',(1.,0.,-5.9211894646675E-14));
#12517=DIRECTION('ref_axis',(0.,1.,0.));
#12518=DIRECTION('center_axis',(1.,0.,0.));
#12519=DIRECTION('ref_axis',(0.,0.707106781186519,-0.707106781186576));
#12520=DIRECTION('',(-1.,0.,0.));
#12521=DIRECTION('',(1.,0.,0.));
#12522=DIRECTION('center_axis',(-0.408248290463859,-0.408248290463835,-0.816496580927742));
#12523=DIRECTION('ref_axis',(-0.577350269189665,-0.577350269189618,0.577350269189594));
#12524=DIRECTION('center_axis',(0.,0.,-1.));
#12525=DIRECTION('ref_axis',(-1.,0.,0.));
#12526=DIRECTION('center_axis',(1.,0.,-5.9211894646675E-14));
#12527=DIRECTION('ref_axis',(0.,-1.,0.));
#12528=DIRECTION('center_axis',(0.,1.,0.));
#12529=DIRECTION('ref_axis',(0.,0.,1.));
#12530=DIRECTION('center_axis',(-0.827465426020388,0.538877990790895,-0.157833709270442));
#12531=DIRECTION('ref_axis',(0.561516668266318,0.794104487760845,-0.232587819494444));
#12532=DIRECTION('center_axis',(0.,-1.,0.));
#12533=DIRECTION('ref_axis',(0.707106781186544,0.,0.707106781186551));
#12534=DIRECTION('center_axis',(-1.,2.96059473233364E-14,0.));
#12535=DIRECTION('ref_axis',(0.,0.,-1.));
#12536=DIRECTION('center_axis',(-0.70710678118657,0.,0.707106781186525));
#12537=DIRECTION('ref_axis',(0.,1.,0.));
#12538=DIRECTION('center_axis',(0.182143211721521,0.879465224064606,0.439732612032315));
#12539=DIRECTION('ref_axis',(0.336556770590777,-0.475963149477983,0.812519920068737));
#12540=DIRECTION('center_axis',(-1.,0.,0.));
#12541=DIRECTION('ref_axis',(0.,0.,1.));
#12542=DIRECTION('center_axis',(0.70710678118654,0.,-0.707106781186555));
#12543=DIRECTION('ref_axis',(0.,-1.,0.));
#12544=DIRECTION('center_axis',(0.,1.,0.));
#12545=DIRECTION('ref_axis',(0.707106781186551,0.,0.707106781186544));
#12546=DIRECTION('center_axis',(-0.408248290463908,0.408248290463861,-0.816496580927704));
#12547=DIRECTION('ref_axis',(-0.577350269189642,0.577350269189594,0.577350269189642));
#12548=DIRECTION('center_axis',(0.,-1.,-5.9211894646675E-14));
#12549=DIRECTION('ref_axis',(-1.,0.,0.));
#12550=DIRECTION('center_axis',(1.,0.,0.));
#12551=DIRECTION('ref_axis',(0.,0.,1.));
#12552=DIRECTION('center_axis',(0.,0.,-1.));
#12553=DIRECTION('ref_axis',(0.,1.,0.));
#12554=DIRECTION('center_axis',(0.,0.,-1.));
#12555=DIRECTION('ref_axis',(-0.707106781186589,0.707106781186506,0.));
#12556=DIRECTION('',(0.,0.,1.));
#12557=DIRECTION('',(0.,0.,-1.));
#12558=DIRECTION('center_axis',(-0.182143211721517,0.879465224064606,-0.439732612032315));
#12559=DIRECTION('ref_axis',(0.336556770590767,0.475963149477992,0.812519920068736));
#12560=DIRECTION('center_axis',(0.,-1.,0.));
#12561=DIRECTION('ref_axis',(0.,0.,1.));
#12562=DIRECTION('center_axis',(0.70710678118654,0.,-0.707106781186555));
#12563=DIRECTION('ref_axis',(0.707106781186555,0.,0.70710678118654));
#12564=DIRECTION('center_axis',(-1.,0.,0.));
#12565=DIRECTION('ref_axis',(0.,1.,0.));
#12566=DIRECTION('center_axis',(1.,0.,0.));
#12567=DIRECTION('ref_axis',(0.,0.707106781186558,0.707106781186537));
#12568=DIRECTION('',(-1.,0.,0.));
#12569=DIRECTION('',(1.,0.,0.));
#12570=DIRECTION('center_axis',(0.707106781186547,0.,-0.707106781186548));
#12571=DIRECTION('ref_axis',(0.499999999999997,0.707106781186559,0.499999999999986));
#12572=DIRECTION('',(-0.707106781186547,0.,0.707106781186548));
#12573=DIRECTION('',(0.707106781186547,0.,-0.707106781186548));
#12574=DIRECTION('center_axis',(0.,1.,0.));
#12575=DIRECTION('ref_axis',(0.382683432365094,0.,0.923879532511285));
#12576=DIRECTION('',(0.,-1.,0.));
#12577=DIRECTION('',(0.,1.,0.));
#12578=DIRECTION('center_axis',(0.,1.,0.));
#12579=DIRECTION('ref_axis',(-0.707106781186558,0.,0.707106781186537));
#12580=DIRECTION('',(0.,-1.,0.));
#12581=DIRECTION('',(0.,1.,0.));
#12582=DIRECTION('center_axis',(-0.707106781186547,0.,0.707106781186548));
#12583=DIRECTION('ref_axis',(0.499999999999997,-0.707106781186559,0.499999999999986));
#12584=DIRECTION('',(0.707106781186547,0.,-0.707106781186548));
#12585=DIRECTION('',(-0.707106781186547,0.,0.707106781186548));
#12586=DIRECTION('center_axis',(-1.,0.,0.));
#12587=DIRECTION('ref_axis',(0.,-0.707106781186558,0.707106781186537));
#12588=DIRECTION('',(1.,0.,0.));
#12589=DIRECTION('',(-1.,0.,0.));
#12590=DIRECTION('center_axis',(-1.,0.,0.));
#12591=DIRECTION('ref_axis',(0.,0.707106781186561,-0.707106781186534));
#12592=DIRECTION('',(-1.,0.,0.));
#12593=DIRECTION('center_axis',(0.,1.,0.));
#12594=DIRECTION('ref_axis',(0.923879532511297,0.,-0.382683432365066));
#12595=DIRECTION('',(0.,1.,0.));
#12596=DIRECTION('center_axis',(0.,0.,-1.));
#12597=DIRECTION('ref_axis',(-0.707106781186506,-0.707106781186589,0.));
#12598=DIRECTION('',(0.,0.,1.));
#12599=DIRECTION('',(0.,0.,-1.));
#12600=DIRECTION('center_axis',(0.,1.,0.));
#12601=DIRECTION('ref_axis',(-0.707106781186519,0.,-0.707106781186576));
#12602=DIRECTION('',(0.,-1.,0.));
#12603=DIRECTION('',(0.,1.,0.));
#12604=DIRECTION('center_axis',(1.,0.,0.));
#12605=DIRECTION('ref_axis',(0.,-0.707106781186561,-0.707106781186534));
#12606=DIRECTION('',(1.,0.,0.));
#12607=DIRECTION('center_axis',(0.,1.,0.));
#12608=DIRECTION('ref_axis',(-0.707106781186519,0.,0.707106781186576));
#12609=DIRECTION('',(0.,-1.,0.));
#12610=DIRECTION('center_axis',(1.,0.,0.));
#12611=DIRECTION('ref_axis',(0.,-0.707106781186561,-0.707106781186534));
#12612=DIRECTION('',(-1.,0.,0.));
#12613=DIRECTION('center_axis',(0.707106781186555,0.,0.70710678118654));
#12614=DIRECTION('ref_axis',(0.70710678118654,0.,-0.707106781186555));
#12615=DIRECTION('',(1.,0.,0.));
#12616=DIRECTION('center_axis',(0.,0.,1.));
#12617=DIRECTION('ref_axis',(0.707106781186506,-0.707106781186589,0.));
#12618=DIRECTION('',(0.,0.,1.));
#12619=DIRECTION('',(0.,0.,-1.));
#12620=DIRECTION('center_axis',(-1.,0.,0.));
#12621=DIRECTION('ref_axis',(0.,0.,-1.));
#12622=DIRECTION('',(0.,-1.,0.));
#12623=DIRECTION('center_axis',(0.,1.,0.));
#12624=DIRECTION('ref_axis',(1.,0.,0.));
#12625=DIRECTION('center_axis',(1.,0.,0.));
#12626=DIRECTION('ref_axis',(0.,0.,1.));
#12627=DIRECTION('center_axis',(0.,0.,-1.));
#12628=DIRECTION('ref_axis',(1.,0.,0.));
#12629=DIRECTION('',(1.,0.,0.));
#12630=DIRECTION('center_axis',(0.,0.,-1.));
#12631=DIRECTION('ref_axis',(1.,0.,0.));
#12632=DIRECTION('',(-1.,0.,0.));
#12633=DIRECTION('center_axis',(0.,0.,-1.));
#12634=DIRECTION('ref_axis',(-1.,0.,0.));
#12635=DIRECTION('center_axis',(-0.707106781186548,0.,-0.707106781186547));
#12636=DIRECTION('ref_axis',(0.707106781186547,0.,-0.707106781186548));
#12637=DIRECTION('center_axis',(0.,1.,0.));
#12638=DIRECTION('ref_axis',(0.,0.,1.));
#12639=DIRECTION('center_axis',(1.,0.,0.));
#12640=DIRECTION('ref_axis',(0.,-0.707106781186516,0.707106781186579));
#12641=DIRECTION('center_axis',(1.,0.,0.));
#12642=DIRECTION('ref_axis',(0.,0.,1.));
#12643=DIRECTION('center_axis',(-1.,0.,0.));
#12644=DIRECTION('ref_axis',(0.,-1.,0.));
#12645=DIRECTION('center_axis',(0.,0.,-1.));
#12646=DIRECTION('ref_axis',(-1.,0.,0.));
#12647=DIRECTION('center_axis',(1.,0.,0.));
#12648=DIRECTION('ref_axis',(0.,1.,0.));
#12649=DIRECTION('center_axis',(0.,0.,1.));
#12650=DIRECTION('ref_axis',(-1.,0.,0.));
#12651=DIRECTION('center_axis',(-1.,0.,0.));
#12652=DIRECTION('ref_axis',(0.,0.707106781186558,0.707106781186537));
#12653=DIRECTION('center_axis',(1.,0.,0.));
#12654=DIRECTION('ref_axis',(0.,1.,0.));
#12655=DIRECTION('',(1.,0.,0.));
#12656=DIRECTION('center_axis',(0.,0.,-1.));
#12657=DIRECTION('ref_axis',(1.,0.,0.));
#12658=DIRECTION('center_axis',(0.,0.,1.));
#12659=DIRECTION('ref_axis',(0.,-1.,0.));
#12660=DIRECTION('',(0.,0.,-1.));
#12661=DIRECTION('center_axis',(0.,1.,0.));
#12662=DIRECTION('ref_axis',(1.,0.,0.));
#12663=DIRECTION('center_axis',(0.,0.,1.));
#12664=DIRECTION('ref_axis',(-1.,0.,0.));
#15415=CARTESIAN_POINT('',(0.,0.,0.));
#15416=CARTESIAN_POINT('Origin',(-69.9040264336917,64.8,3.08953555269655));
#15417=CARTESIAN_POINT('',(-104.475451921837,64.8,2.78953555269655));
#15418=CARTESIAN_POINT('',(-104.475451921837,64.5,3.08953555269655));
#15419=CARTESIAN_POINT('Origin',(-104.475451921837,64.8,3.08953555269655));
#15420=CARTESIAN_POINT('',(-77.8080528673835,64.8,2.78953555269655));
#15421=CARTESIAN_POINT('',(-69.9040264336917,64.8,2.78953555269655));
#15422=CARTESIAN_POINT('',(-77.8080528673835,64.5,3.08953555269655));
#15423=CARTESIAN_POINT('Origin',(-77.8080528673835,64.8,3.08953555269655));
#15424=CARTESIAN_POINT('',(-69.9040264336917,64.5,3.08953555269655));
#15425=CARTESIAN_POINT('Origin',(-77.8080528673835,60.,3.08953555269655));
#15426=CARTESIAN_POINT('',(-77.8080528673835,55.5,3.08953555269655));
#15427=CARTESIAN_POINT('',(-77.8080528673835,55.2,2.78953555269655));
#15428=CARTESIAN_POINT('Origin',(-77.8080528673835,55.2,3.08953555269655));
#15429=CARTESIAN_POINT('Origin',(-77.8080528673835,60.,3.08953555269655));
#15430=CARTESIAN_POINT('Origin',(-77.8080528673835,60.,2.78953555269655));
#15431=CARTESIAN_POINT('Origin',(-83.2377259609183,55.2,3.08953555269655));
#15432=CARTESIAN_POINT('',(-104.475451921837,55.5,3.08953555269655));
#15433=CARTESIAN_POINT('',(-104.475451921837,55.2,2.78953555269655));
#15434=CARTESIAN_POINT('Origin',(-104.475451921837,55.2,3.08953555269655));
#15435=CARTESIAN_POINT('',(-83.2377259609183,55.5,3.08953555269655));
#15436=CARTESIAN_POINT('',(-83.2377259609183,55.2,2.78953555269655));
#15437=CARTESIAN_POINT('Origin',(-104.475451921837,60.,3.08953555269655));
#15438=CARTESIAN_POINT('Origin',(-104.475451921837,60.,3.08953555269655));
#15439=CARTESIAN_POINT('Origin',(-104.475451921837,60.,2.78953555269655));
#15440=CARTESIAN_POINT('Origin',(-77.8080528673835,60.,10.7895355526966));
#15441=CARTESIAN_POINT('',(-77.8080528673835,55.5,10.4895355526966));
#15442=CARTESIAN_POINT('',(-77.8080528673835,55.5,10.7895355526966));
#15443=CARTESIAN_POINT('',(-77.8080528673835,64.5,10.4895355526966));
#15444=CARTESIAN_POINT('Origin',(-77.8080528673835,60.,10.4895355526966));
#15445=CARTESIAN_POINT('',(-77.8080528673835,64.5,10.7895355526966));
#15446=CARTESIAN_POINT('Origin',(-77.8080528673835,64.5,10.7895355526966));
#15447=CARTESIAN_POINT('',(-104.475451921837,64.5,10.4895355526966));
#15448=CARTESIAN_POINT('',(-94.9040264336917,64.5,10.4895355526966));
#15449=CARTESIAN_POINT('',(-104.475451921837,64.5,10.7895355526966));
#15450=CARTESIAN_POINT('Origin',(-62.,70.,2.78953555269655));
#15451=CARTESIAN_POINT('',(-109.7,69.7,2.78953555269655));
#15452=CARTESIAN_POINT('',(-62.7242640687119,69.7,2.78953555269655));
#15453=CARTESIAN_POINT('',(-74.5,69.7,2.78953555269655));
#15454=CARTESIAN_POINT('',(-62.7242640687119,50.3,2.78953555269655));
#15455=CARTESIAN_POINT('',(-62.7242640687119,70.,2.78953555269655));
#15456=CARTESIAN_POINT('',(-109.7,50.3,2.78953555269655));
#15457=CARTESIAN_POINT('',(-74.5,50.3,2.78953555269655));
#15458=CARTESIAN_POINT('',(-109.7,70.,2.78953555269655));
#15459=CARTESIAN_POINT('Origin',(-109.7,50.3,2.48953555269655));
#15460=CARTESIAN_POINT('',(-109.7,50.,3.08953555269655));
#15461=CARTESIAN_POINT('Origin',(-109.7,50.3,3.08953555269655));
#15462=CARTESIAN_POINT('',(-110.3,50.,2.48953555269655));
#15463=CARTESIAN_POINT('Origin',(-109.7,50.,2.48953555269655));
#15464=CARTESIAN_POINT('',(-110.,50.3,2.48953555269655));
#15465=CARTESIAN_POINT('Origin',(-110.3,50.3,2.48953555269655));
#15466=CARTESIAN_POINT('Origin',(-109.7,50.3,2.48953555269655));
#15467=CARTESIAN_POINT('Origin',(-111.7,50.3,0.3));
#15468=CARTESIAN_POINT('',(-111.7,50.3,0.));
#15469=CARTESIAN_POINT('',(-111.7,50.,0.3));
#15470=CARTESIAN_POINT('Origin',(-111.7,50.3,0.3));
#15471=CARTESIAN_POINT('',(-112.,50.3,0.3));
#15472=CARTESIAN_POINT('Origin',(-111.7,50.3,0.3));
#15473=CARTESIAN_POINT('Origin',(-111.7,50.3,0.3));
#15474=CARTESIAN_POINT('Origin',(-109.7,69.7,2.48953555269655));
#15475=CARTESIAN_POINT('',(-109.7,70.,3.08953555269655));
#15476=CARTESIAN_POINT('',(-110.3,70.,2.48953555269655));
#15477=CARTESIAN_POINT('Origin',(-109.7,70.,2.48953555269655));
#15478=CARTESIAN_POINT('Origin',(-109.7,69.7,3.08953555269655));
#15479=CARTESIAN_POINT('',(-110.,69.7,2.48953555269655));
#15480=CARTESIAN_POINT('Origin',(-109.7,69.7,2.48953555269655));
#15481=CARTESIAN_POINT('Origin',(-110.3,69.7,2.48953555269655));
#15482=CARTESIAN_POINT('Origin',(-110.3,69.7,4.09215166452241));
#15483=CARTESIAN_POINT('',(-110.,69.7,0.));
#15484=CARTESIAN_POINT('',(-110.,69.7,4.09215166452241));
#15485=CARTESIAN_POINT('',(-110.3,70.,0.3));
#15486=CARTESIAN_POINT('Origin',(-110.3,69.7,0.3));
#15487=CARTESIAN_POINT('',(-110.3,70.,4.09215166452241));
#15488=CARTESIAN_POINT('Origin',(-62.7242640687119,50.3,3.08953555269655));
#15489=CARTESIAN_POINT('',(-62.512132034356,50.3,3.30166758705252));
#15490=CARTESIAN_POINT('',(-62.7242640687119,50.,3.08953555269655));
#15491=CARTESIAN_POINT('Origin',(-62.7242640687119,50.3,3.08953555269656));
#15492=CARTESIAN_POINT('Origin',(-62.7242640687119,50.3,3.08953555269655));
#15493=CARTESIAN_POINT('Origin',(-62.7242640687119,50.3,3.08953555269655));
#15494=CARTESIAN_POINT('Origin',(-111.7,69.7,0.3));
#15495=CARTESIAN_POINT('',(-111.7,69.7,0.));
#15496=CARTESIAN_POINT('',(-112.,69.7,0.3));
#15497=CARTESIAN_POINT('Origin',(-111.7,69.7,0.3));
#15498=CARTESIAN_POINT('',(-111.7,70.,0.3));
#15499=CARTESIAN_POINT('Origin',(-111.7,69.7,0.3));
#15500=CARTESIAN_POINT('Origin',(-111.7,69.7,0.3));
#15501=CARTESIAN_POINT('Origin',(-98.5,69.7,0.3));
#15502=CARTESIAN_POINT('',(-98.5,70.,0.3));
#15503=CARTESIAN_POINT('',(-98.5,69.7,0.));
#15504=CARTESIAN_POINT('Origin',(-111.7,50.3,10.4895355526966));
#15505=CARTESIAN_POINT('',(-112.,50.3,10.4895355526966));
#15506=CARTESIAN_POINT('',(-111.7,50.,10.4895355526966));
#15507=CARTESIAN_POINT('Origin',(-111.7,50.3,10.4895355526966));
#15508=CARTESIAN_POINT('',(-111.7,50.3,10.7895355526966));
#15509=CARTESIAN_POINT('Origin',(-111.7,50.3,10.4895355526966));
#15510=CARTESIAN_POINT('Origin',(-111.7,50.3,10.4895355526966));
#15511=CARTESIAN_POINT('Origin',(-62.7242640687119,69.7,3.08953555269655));
#15512=CARTESIAN_POINT('',(-62.512132034356,69.7,3.30166758705252));
#15513=CARTESIAN_POINT('Origin',(-62.7242640687119,69.7,3.08953555269655));
#15514=CARTESIAN_POINT('',(-62.7242640687119,70.,3.08953555269655));
#15515=CARTESIAN_POINT('Origin',(-62.7242640687119,69.7,3.08953555269655));
#15516=CARTESIAN_POINT('Origin',(-62.7242640687119,69.7,3.08953555269655));
#15517=CARTESIAN_POINT('Origin',(-70.1242640687119,50.3,10.4895355526966));
#15518=CARTESIAN_POINT('',(-70.1242640687119,50.3,10.7895355526966));
#15519=CARTESIAN_POINT('',(-70.1242640687119,50.,10.4895355526966));
#15520=CARTESIAN_POINT('Origin',(-70.1242640687119,50.3,10.4895355526966));
#15521=CARTESIAN_POINT('',(-69.9121320343559,50.3,10.7016675870525));
#15522=CARTESIAN_POINT('Origin',(-70.1242640687119,50.3,10.4895355526966));
#15523=CARTESIAN_POINT('Origin',(-70.1242640687119,50.3,10.4895355526966));
#15524=CARTESIAN_POINT('Origin',(-111.7,69.7,10.4895355526966));
#15525=CARTESIAN_POINT('',(-112.,69.7,10.4895355526966));
#15526=CARTESIAN_POINT('',(-111.7,69.7,10.7895355526966));
#15527=CARTESIAN_POINT('Origin',(-111.7,69.7,10.4895355526966));
#15528=CARTESIAN_POINT('',(-111.7,70.,10.4895355526966));
#15529=CARTESIAN_POINT('Origin',(-111.7,69.7,10.4895355526966));
#15530=CARTESIAN_POINT('Origin',(-111.7,69.7,10.4895355526966));
#15531=CARTESIAN_POINT('Origin',(-111.7,69.7,2.69738388817414));
#15532=CARTESIAN_POINT('',(-111.7,70.,2.69738388817414));
#15533=CARTESIAN_POINT('',(-112.,69.7,2.69738388817414));
#15534=CARTESIAN_POINT('Origin',(-70.1242640687119,69.7,10.4895355526966));
#15535=CARTESIAN_POINT('',(-70.1242640687119,69.7,10.7895355526966));
#15536=CARTESIAN_POINT('',(-69.9121320343559,69.7,10.7016675870525));
#15537=CARTESIAN_POINT('Origin',(-70.1242640687119,69.7,10.4895355526966));
#15538=CARTESIAN_POINT('',(-70.1242640687119,70.,10.4895355526966));
#15539=CARTESIAN_POINT('Origin',(-70.1242640687119,69.7,10.4895355526966));
#15540=CARTESIAN_POINT('Origin',(-70.1242640687119,69.7,10.4895355526966));
#15541=CARTESIAN_POINT('Origin',(-99.5,69.7,10.4895355526966));
#15542=CARTESIAN_POINT('',(-99.5,69.7,10.7895355526966));
#15543=CARTESIAN_POINT('',(-99.5,70.,10.4895355526966));
#15544=CARTESIAN_POINT('Origin',(-73.1134400902689,69.7,13.4787115742535));
#15545=CARTESIAN_POINT('',(-72.9013080559129,69.7,13.6908436086095));
#15546=CARTESIAN_POINT('',(-73.1134400902689,70.,13.4787115742535));
#15547=CARTESIAN_POINT('Origin',(-70.1242640687119,70.,10.4895355526966));
#15548=CARTESIAN_POINT('',(-69.9121320343559,70.,10.7016675870525));
#15549=CARTESIAN_POINT('',(-70.1242640687119,70.,10.7895355526966));
#15550=CARTESIAN_POINT('Origin',(-111.7,70.,10.4895355526966));
#15551=CARTESIAN_POINT('',(-111.7,70.,10.7895355526966));
#15552=CARTESIAN_POINT('',(-112.,70.,10.4895355526966));
#15553=CARTESIAN_POINT('Origin',(-73.1134400902689,50.3,13.4787115742535));
#15554=CARTESIAN_POINT('',(-72.9013080559129,50.3,13.6908436086095));
#15555=CARTESIAN_POINT('',(-73.1134400902689,50.,13.4787115742535));
#15556=CARTESIAN_POINT('Origin',(-99.5,50.3,10.4895355526966));
#15557=CARTESIAN_POINT('',(-99.5,50.3,10.7895355526966));
#15558=CARTESIAN_POINT('',(-99.5,50.,10.4895355526966));
#15559=CARTESIAN_POINT('Origin',(-74.5,69.7,3.08953555269655));
#15560=CARTESIAN_POINT('',(-74.5,70.,3.08953555269655));
#15561=CARTESIAN_POINT('Origin',(-62.7242640687119,70.,3.08953555269655));
#15562=CARTESIAN_POINT('',(-62.512132034356,70.,3.30166758705252));
#15563=CARTESIAN_POINT('Origin',(-111.7,50.3,2.69738388817414));
#15564=CARTESIAN_POINT('',(-112.,50.3,2.69738388817414));
#15565=CARTESIAN_POINT('',(-111.7,50.,2.69738388817414));
#15566=CARTESIAN_POINT('Origin',(-111.7,70.,0.3));
#15567=CARTESIAN_POINT('',(-112.,70.,0.3));
#15568=CARTESIAN_POINT('',(-111.7,70.,0.));
#15569=CARTESIAN_POINT('Origin',(-74.5,50.3,3.08953555269655));
#15570=CARTESIAN_POINT('',(-74.5,50.,3.08953555269655));
#15571=CARTESIAN_POINT('Origin',(-109.7,70.,2.48953555269655));
#15572=CARTESIAN_POINT('',(-110.,70.,2.48953555269655));
#15573=CARTESIAN_POINT('Origin',(-98.5,50.3,0.3));
#15574=CARTESIAN_POINT('',(-110.,50.3,0.));
#15575=CARTESIAN_POINT('',(-98.5,50.3,0.));
#15576=CARTESIAN_POINT('',(-110.3,50.,0.3));
#15577=CARTESIAN_POINT('Origin',(-110.3,50.3,0.3));
#15578=CARTESIAN_POINT('',(-98.5,50.,0.3));
#15579=CARTESIAN_POINT('Origin',(-110.3,50.3,4.09215166452241));
#15580=CARTESIAN_POINT('',(-110.3,50.,4.09215166452241));
#15581=CARTESIAN_POINT('',(-110.,50.3,4.09215166452241));
#15582=CARTESIAN_POINT('Origin',(-110.,70.,2.78953555269655));
#15583=CARTESIAN_POINT('',(-110.,70.,0.));
#15584=CARTESIAN_POINT('Origin',(-87.,70.,5.39476777634828));
#15585=CARTESIAN_POINT('Origin',(-112.,70.,0.));
#15586=CARTESIAN_POINT('Origin',(-112.,70.,10.7895355526966));
#15587=CARTESIAN_POINT('',(-104.475451921837,64.8,10.7895355526966));
#15588=CARTESIAN_POINT('',(-77.8080528673835,64.8,10.7895355526966));
#15589=CARTESIAN_POINT('',(-94.9040264336917,64.8,10.7895355526966));
#15590=CARTESIAN_POINT('',(-77.8080528673835,55.2,10.7895355526966));
#15591=CARTESIAN_POINT('Origin',(-77.8080528673835,60.,10.7895355526966));
#15592=CARTESIAN_POINT('',(-104.475451921837,55.2,10.7895355526966));
#15593=CARTESIAN_POINT('',(-108.237725960918,55.2,10.7895355526966));
#15594=CARTESIAN_POINT('Origin',(-104.475451921837,60.,10.7895355526966));
#15595=CARTESIAN_POINT('Origin',(-70.,70.,10.7895355526965));
#15596=CARTESIAN_POINT('Origin',(-87.,50.,5.39476777634828));
#15597=CARTESIAN_POINT('Origin',(-94.9040264336917,64.8,10.4895355526966));
#15598=CARTESIAN_POINT('Origin',(-77.8080528673835,64.8,10.4895355526966));
#15599=CARTESIAN_POINT('Origin',(-104.475451921837,64.8,10.4895355526966));
#15600=CARTESIAN_POINT('Origin',(-104.475451921837,60.,10.4895355526966));
#15601=CARTESIAN_POINT('',(-104.475451921837,55.5,10.4895355526966));
#15602=CARTESIAN_POINT('Origin',(-104.475451921837,55.2,10.4895355526966));
#15603=CARTESIAN_POINT('Origin',(-104.475451921837,60.,10.4895355526966));
#15604=CARTESIAN_POINT('Origin',(-108.237725960918,55.2,10.4895355526966));
#15605=CARTESIAN_POINT('Origin',(-77.8080528673835,55.2,10.4895355526966));
#15606=CARTESIAN_POINT('',(-108.237725960918,55.5,10.4895355526966));
#15607=CARTESIAN_POINT('Origin',(-77.8080528673835,60.,10.4895355526966));
#15608=CARTESIAN_POINT('Origin',(-104.475451921837,60.,10.7895355526966));
#15609=CARTESIAN_POINT('',(-104.475451921837,55.5,10.7895355526966));
#15610=CARTESIAN_POINT('Origin',(-104.475451921837,55.5,10.7895355526966));
#15611=CARTESIAN_POINT('Origin',(-110.,70.,0.));
#17818=UNCERTAINTY_MEASURE_WITH_UNIT(LENGTH_MEASURE(0.01),#17837,
'DISTANCE_ACCURACY_VALUE',
'Maximum model space distance between geometric entities at asserted c
onnectivities');
#17824=UNCERTAINTY_MEASURE_WITH_UNIT(LENGTH_MEASURE(0.01),#17837,
'DISTANCE_ACCURACY_VALUE',
'Maximum model space distance between geometric entities at asserted c
onnectivities');
#17830=(
GEOMETRIC_REPRESENTATION_CONTEXT(3)
GLOBAL_UNCERTAINTY_ASSIGNED_CONTEXT((#17818))
GLOBAL_UNIT_ASSIGNED_CONTEXT((#17837,#17839,#17840))
REPRESENTATION_CONTEXT('','3D')
);
#17836=(
GEOMETRIC_REPRESENTATION_CONTEXT(3)
GLOBAL_UNCERTAINTY_ASSIGNED_CONTEXT((#17824))
GLOBAL_UNIT_ASSIGNED_CONTEXT((#17837,#17839,#17840))
REPRESENTATION_CONTEXT('','3D')
);
#17837=(
LENGTH_UNIT()
NAMED_UNIT(*)
SI_UNIT(.MILLI.,.METRE.)
);
#17839=(
NAMED_UNIT(*)
PLANE_ANGLE_UNIT()
SI_UNIT($,.RADIAN.)
);
#17840=(
NAMED_UNIT(*)
SI_UNIT($,.STERADIAN.)
SOLID_ANGLE_UNIT()
);
#17846=SHAPE_DEFINITION_REPRESENTATION(#17857,#17878);
#17857=PRODUCT_DEFINITION_SHAPE('',$,#17890);
#17878=SHAPE_REPRESENTATION('',(#10301),#17830);
#17884=PRODUCT_DEFINITION_CONTEXT('part definition',#17919,'design');
#17890=PRODUCT_DEFINITION('Clamp_02','Clamp_02',#17901,#17884);
#17901=PRODUCT_DEFINITION_FORMATION('',$,#17926);
#17919=APPLICATION_CONTEXT(
'Core Data for Automotive Mechanical Design Process');
#17920=PRODUCT_CONTEXT('part definition',#17919,'mechanical');
#17926=PRODUCT('Clamp_02','Clamp_02',$,(#17920));
#17981=COLOUR_RGB('Off White',0.89,0.88,0.83);
#17982=FILL_AREA_STYLE_COLOUR('',#17981);
#17983=FILL_AREA_STYLE('',(#17982));
#17984=SURFACE_STYLE_FILL_AREA(#17983);
#17985=SURFACE_SIDE_STYLE('',(#17984));
#17986=SURFACE_STYLE_USAGE(.BOTH.,#17985);
#17987=PRESENTATION_STYLE_ASSIGNMENT((#17986));
ENDSEC;
END-ISO-10303-21;
